ISO-10303-21;
HEADER;
FILE_DESCRIPTION (('STEP AP214'),
    '1' );
FILE_NAME ('socket head cap screw_iso_ISO 4762 M8 x 35 - 35N.step',
    '2026-10-26T22:46:44',
    ( '' ),
    ( '' ),
    'SwSTEP 2.0',
    'SolidWorks 2025',
    '' );
FILE_SCHEMA (( 'AUTOMOTIVE_DESIGN' ));
ENDSEC;

DATA;
#28=DIRECTION ( 'NONE',  ( -0.000000000000000000, 1.355657144061424088E-15, 1.000000000000000000 ) ) ;
#45=CARTESIAN_POINT ( 'NONE',  ( 43.00000000000000000, 0.000000000000000000, 0.000000000000000000 ) ) ;
#71=ORIENTED_EDGE ( 'NONE', *, *, #7515, .F. ) ;
#73=DIRECTION ( 'NONE',  ( -1.000000000000000000, -0.000000000000000000, -0.000000000000000000 ) ) ;
#81=AXIS2_PLACEMENT_3D ( 'NONE', #9573, #7982, #13089 ) ;
#111=LINE ( 'NONE', #3275, #10000 ) ;
#129=DIRECTION ( 'NONE',  ( 0.000000000000000000, -0.5000000000000009992, -0.8660254037844380415 ) ) ;
#130=CARTESIAN_POINT ( 'NONE',  ( 43.00000000000000000, 4.052968581778165278E-16, -3.309499999999999886 ) ) ;
#140=VERTEX_POINT ( 'NONE', #15368 ) ;
#146=DIRECTION ( 'NONE',  ( -1.000000000000000000, -0.000000000000000000, -0.000000000000000000 ) ) ;
#213=CIRCLE ( 'NONE', #14445, 0.4000000000000001887 ) ;
#221=CIRCLE ( 'NONE', #10696, 3.047499999999999876 ) ;
#241=AXIS2_PLACEMENT_3D ( 'NONE', #8090, #7996, #6604 ) ;
#256=DIRECTION ( 'NONE',  ( 1.000000000000000000, 0.000000000000000000, 0.000000000000000000 ) ) ;
#261=CARTESIAN_POINT ( 'NONE',  ( 4.000000000000000000, 1.759474945355379960, -3.047500000000001652 ) ) ;
#326=ORIENTED_EDGE ( 'NONE', *, *, #16117, .T. ) ;
#331=CARTESIAN_POINT ( 'NONE',  ( 0.000000000000000000, 3.518949890710767026, -4.987329993433320396E-15 ) ) ;
#333=DIRECTION ( 'NONE',  ( 0.000000000000000000, 0.8660254037844380415, -0.5000000000000009992 ) ) ;
#376=EDGE_CURVE ( 'NONE', #7292, #12993, #6301, .T. ) ;
#423=VERTEX_POINT ( 'NONE', #6399 ) ;
#431=ORIENTED_EDGE ( 'NONE', *, *, #6280, .F. ) ;
#439=DIRECTION ( 'NONE',  ( 0.000000000000000000, 0.000000000000000000, 1.000000000000000000 ) ) ;
#471=AXIS2_PLACEMENT_3D ( 'NONE', #2230, #11878, #3809 ) ;
#475=EDGE_CURVE ( 'NONE', #17447, #7969, #486, .T. ) ;
#486=LINE ( 'NONE', #5128, #4264 ) ;
#503=ORIENTED_EDGE ( 'NONE', *, *, #7221, .T. ) ;
#505=CIRCLE ( 'NONE', #3203, 0.4000000000000001887 ) ;
#559=EDGE_LOOP ( 'NONE', ( #3305, #9040, #19379, #13830, #16196 ) ) ;
#560=DIRECTION ( 'NONE',  ( 0.000000000000000000, 0.000000000000000000, 1.000000000000000000 ) ) ;
#565=PLANE ( 'NONE',  #13550 ) ;
#592=CIRCLE ( 'NONE', #20223, 6.099999999999999645 ) ;
#602=ORIENTED_EDGE ( 'NONE', *, *, #8700, .T. ) ;
#645=EDGE_LOOP ( 'NONE', ( #9924, #18297, #15540 ) ) ;
#647=FACE_OUTER_BOUND ( 'NONE', #11082, .T. ) ;
#676=CARTESIAN_POINT ( 'NONE',  ( 4.000000000000000000, 1.759474945355388398, 3.047499999999996767 ) ) ;
#678=DIRECTION ( 'NONE',  ( -1.000000000000000000, -0.000000000000000000, -0.000000000000000000 ) ) ;
#729=ADVANCED_FACE ( 'NONE', ( #7768 ), #11059, .T. ) ;
#763=EDGE_CURVE ( 'NONE', #7000, #12336, #221, .T. ) ;
#790=ORIENTED_EDGE ( 'NONE', *, *, #8700, .F. ) ;
#833=EDGE_CURVE ( 'NONE', #12601, #7000, #19833, .T. ) ;
#867=CARTESIAN_POINT ( 'NONE',  ( 4.000000000000000000, 1.759474945355379960, -3.047500000000001652 ) ) ;
#885=DIRECTION ( 'NONE',  ( -1.000000000000000000, -0.000000000000000000, -0.000000000000000000 ) ) ;
#913=ORIENTED_EDGE ( 'NONE', *, *, #13556, .T. ) ;
#921=DIRECTION ( 'NONE',  ( -1.000000000000000000, -0.000000000000000000, -0.000000000000000000 ) ) ;
#927=APPLICATION_CONTEXT ( 'automotive_design' ) ;
#996=LINE ( 'NONE', #10624, #19259 ) ;
#1044=EDGE_LOOP ( 'NONE', ( #913, #16767, #17162, #15739, #1155 ) ) ;
#1109=ORIENTED_EDGE ( 'NONE', *, *, #16804, .T. ) ;
#1115=VECTOR ( 'NONE', #8761, 1000.000000000000227 ) ;
#1155=ORIENTED_EDGE ( 'NONE', *, *, #17981, .T. ) ;
#1268=PLANE ( 'NONE',  #18508 ) ;
#1273=ADVANCED_FACE ( 'NONE', ( #7094 ), #3386, .T. ) ;
#1274=DIRECTION ( 'NONE',  ( 0.000000000000000000, 0.000000000000000000, 1.000000000000000000 ) ) ;
#1287=CARTESIAN_POINT ( 'NONE',  ( 4.000000000000000000, 5.278424836066145431, -3.047500000000006093 ) ) ;
#1310=DIRECTION ( 'NONE',  ( -1.000000000000000000, -0.000000000000000000, -0.000000000000000000 ) ) ;
#1364=VERTEX_POINT ( 'NONE', #7201 ) ;
#1368=DIRECTION ( 'NONE',  ( 0.000000000000000000, -0.4999999999999985012, 0.8660254037844394848 ) ) ;
#1418=AXIS2_PLACEMENT_3D ( 'NONE', #17347, #9265, #19043 ) ;
#1442=CIRCLE ( 'NONE', #14325, 4.400000000000000355 ) ;
#1505=CARTESIAN_POINT ( 'NONE',  ( 4.000000000000000000, 3.518949890710767026, -4.987329993433320396E-15 ) ) ;
#1547=AXIS2_PLACEMENT_3D ( 'NONE', #1922, #11882, #19602 ) ;
#1564=ORIENTED_EDGE ( 'NONE', *, *, #13958, .F. ) ;
#1578=ORIENTED_EDGE ( 'NONE', *, *, #7221, .F. ) ;
#1580=LINE ( 'NONE', #6016, #13806 ) ;
#1590=DIRECTION ( 'NONE',  ( -1.000000000000000000, -0.000000000000000000, -0.000000000000000000 ) ) ;
#1600=ORIENTED_EDGE ( 'NONE', *, *, #16947, .T. ) ;
#1604=ORIENTED_EDGE ( 'NONE', *, *, #6782, .T. ) ;
#1611=CARTESIAN_POINT ( 'NONE',  ( 4.000000000000000000, 2.639212418033074048, -1.523750000000002602 ) ) ;
#1660=ORIENTED_EDGE ( 'NONE', *, *, #12462, .F. ) ;
#1678=FACE_OUTER_BOUND ( 'NONE', #15463, .T. ) ;
#1735=CARTESIAN_POINT ( 'NONE',  ( 0.3999999999999975797, 7.470345474798854293E-16, -6.099999999999999645 ) ) ;
#1811=VERTEX_POINT ( 'NONE', #9149 ) ;
#1859=VECTOR ( 'NONE', #19529, 1000.000000000000000 ) ;
#1903=CARTESIAN_POINT ( 'NONE',  ( 8.399999999999998579, 5.388445916248354013E-16, 4.400000000000000355 ) ) ;
#1922=CARTESIAN_POINT ( 'NONE',  ( 43.00000000000000000, 0.000000000000000000, 0.000000000000000000 ) ) ;
#1923=EDGE_CURVE ( 'NONE', #7969, #18781, #17221, .T. ) ;
#1986=EDGE_CURVE ( 'NONE', #18021, #17954, #14691, .T. ) ;
#2033=EDGE_CURVE ( 'NONE', #6599, #17447, #17091, .T. ) ;
#2042=AXIS2_PLACEMENT_3D ( 'NONE', #2483, #885, #7334 ) ;
#2048=EDGE_CURVE ( 'NONE', #11211, #14920, #505, .T. ) ;
#2061=CIRCLE ( 'NONE', #17299, 3.047499999999999876 ) ;
#2074=VECTOR ( 'NONE', #13166, 999.9999999999998863 ) ;
#2078=CIRCLE ( 'NONE', #13934, 0.4000000000000001887 ) ;
#2088=DIRECTION ( 'NONE',  ( 0.000000000000000000, 0.000000000000000000, 1.000000000000000000 ) ) ;
#2097=ORIENTED_EDGE ( 'NONE', *, *, #475, .F. ) ;
#2117=ORIENTED_EDGE ( 'NONE', *, *, #6280, .T. ) ;
#2122=EDGE_LOOP ( 'NONE', ( #5272, #18553 ) ) ;
#2151=EDGE_LOOP ( 'NONE', ( #15487, #12873, #8459, #9810, #18958 ) ) ;
#2207=ADVANCED_FACE ( 'NONE', ( #20160 ), #565, .F. ) ;
#2228=ORIENTED_EDGE ( 'NONE', *, *, #7798, .T. ) ;
#2230=CARTESIAN_POINT ( 'NONE',  ( 43.00000000000000000, 3.309499999999999886, 0.000000000000000000 ) ) ;
#2253=CARTESIAN_POINT ( 'NONE',  ( 4.000000000000000000, 0.000000000000000000, 0.000000000000000000 ) ) ;
#2321=( GEOMETRIC_REPRESENTATION_CONTEXT ( 3 ) GLOBAL_UNCERTAINTY_ASSIGNED_CONTEXT ( ( #10843 ) ) GLOBAL_UNIT_ASSIGNED_CONTEXT ( ( #20398, #10971, #10854 ) ) REPRESENTATION_CONTEXT ( 'NONE', 'WORKASPACE' ) );
#2406=LINE ( 'NONE', #15050, #8892 ) ;
#2419=DIRECTION ( 'NONE',  ( -1.000000000000000000, -0.000000000000000000, -0.000000000000000000 ) ) ;
#2449=DIRECTION ( 'NONE',  ( 0.000000000000000000, 0.8660254037844381525, -0.5000000000000009992 ) ) ;
#2455=CARTESIAN_POINT ( 'NONE',  ( 42.30949999999999989, 4.898587196589411843E-16, -3.999999999999999112 ) ) ;
#2478=ADVANCED_FACE ( 'NONE', ( #8049 ), #6456, .T. ) ;
#2483=CARTESIAN_POINT ( 'NONE',  ( 0.3999999999999975797, 0.000000000000000000, 0.000000000000000000 ) ) ;
#2492=ORIENTED_EDGE ( 'NONE', *, *, #15628, .T. ) ;
#2534=EDGE_LOOP ( 'NONE', ( #431, #7158, #8019, #1564 ) ) ;
#2569=VERTEX_POINT ( 'NONE', #16311 ) ;
#2585=DIRECTION ( 'NONE',  ( 0.000000000000000000, 0.000000000000000000, 1.000000000000000000 ) ) ;
#2603=VECTOR ( 'NONE', #5241, 1000.000000000000000 ) ;
#2630=( LENGTH_UNIT ( ) NAMED_UNIT ( * ) SI_UNIT ( .MILLI., .METRE. ) );
#2656=CIRCLE ( 'NONE', #11787, 6.500000000000000000 ) ;
#2728=DIRECTION ( 'NONE',  ( 0.000000000000000000, -0.5000000000000009992, -0.8660254037844380415 ) ) ;
#2747=VECTOR ( 'NONE', #1310, 1000.000000000000000 ) ;
#2751=FACE_OUTER_BOUND ( 'NONE', #8635, .T. ) ;
#2771=DIRECTION ( 'NONE',  ( 1.000000000000000000, 0.000000000000000000, 0.000000000000000000 ) ) ;
#2783=EDGE_LOOP ( 'NONE', ( #11949, #13867, #12411, #8559 ) ) ;
#2785=CARTESIAN_POINT ( 'NONE',  ( 0.3999999999999975797, 0.000000000000000000, 6.500000000000000000 ) ) ;
#2790=CARTESIAN_POINT ( 'NONE',  ( 4.000000000000000000, 0.000000000000000000, 0.000000000000000000 ) ) ;
#2800=CARTESIAN_POINT ( 'NONE',  ( 4.000000000000000000, 1.759474945355379960, -3.047500000000001652 ) ) ;
#2801=ADVANCED_FACE ( 'NONE', ( #13974 ), #12275, .T. ) ;
#2871=DIRECTION ( 'NONE',  ( 0.000000000000000000, -1.000000000000000000, 1.232415585510385534E-15 ) ) ;
#2920=CARTESIAN_POINT ( 'NONE',  ( 0.000000000000000000, 0.000000000000000000, 0.000000000000000000 ) ) ;
#2959=DIRECTION ( 'NONE',  ( -0.000000000000000000, 0.8660254037844394848, 0.4999999999999985012 ) ) ;
#2967=DIRECTION ( 'NONE',  ( 0.000000000000000000, 0.000000000000000000, 1.000000000000000000 ) ) ;
#3009=CARTESIAN_POINT ( 'NONE',  ( 43.00000000000000000, 0.000000000000000000, 0.000000000000000000 ) ) ;
#3087=EDGE_CURVE ( 'NONE', #11275, #12336, #16583, .T. ) ;
#3126=DIRECTION ( 'NONE',  ( 0.000000000000000000, 0.000000000000000000, 1.000000000000000000 ) ) ;
#3149=CARTESIAN_POINT ( 'NONE',  ( 4.000000000000000000, -1.759474945355379072, 3.047500000000001652 ) ) ;
#3203=AXIS2_PLACEMENT_3D ( 'NONE', #1735, #3322, #8075 ) ;
#3211=UNCERTAINTY_MEASURE_WITH_UNIT (LENGTH_MEASURE( 1.000000000000000082E-05 ), #2630, 'distance_accuracy_value', 'NONE');
#3215=EDGE_CURVE ( 'NONE', #20478, #12601, #15337, .T. ) ;
#3263=DIRECTION ( 'NONE',  ( 1.000000000000000000, 0.000000000000000000, 0.000000000000000000 ) ) ;
#3264=ORIENTED_EDGE ( 'NONE', *, *, #12504, .T. ) ;
#3275=CARTESIAN_POINT ( 'NONE',  ( -31.74999999999995737, 0.000000000000000000, 6.500000000000000000 ) ) ;
#3305=ORIENTED_EDGE ( 'NONE', *, *, #7798, .F. ) ;
#3322=DIRECTION ( 'NONE',  ( -0.000000000000000000, 1.000000000000000000, 1.224646799147353207E-16 ) ) ;
#3375=CARTESIAN_POINT ( 'NONE',  ( 4.000000000000000000, -3.518949890710766581, 4.553649124439118623E-15 ) ) ;
#3386=PLANE ( 'NONE',  #471 ) ;
#3435=CARTESIAN_POINT ( 'NONE',  ( 4.000000000000000000, 5.278424836066145431, -3.047500000000006093 ) ) ;
#3452=VERTEX_POINT ( 'NONE', #20297 ) ;
#3456=CONICAL_SURFACE ( 'NONE', #15339, 3.047499999999999876, 1.047197551196590748 ) ;
#3460=DIRECTION ( 'NONE',  ( -1.000000000000000000, -0.000000000000000000, -0.000000000000000000 ) ) ;
#3463=ORIENTED_EDGE ( 'NONE', *, *, #13556, .F. ) ;
#3496=DIRECTION ( 'NONE',  ( 0.000000000000000000, 0.000000000000000000, -1.000000000000000000 ) ) ;
#3505=DIRECTION ( 'NONE',  ( -1.000000000000000000, -0.000000000000000000, -0.000000000000000000 ) ) ;
#3537=EDGE_LOOP ( 'NONE', ( #2492, #12281, #5509, #3824 ) ) ;
#3554=DIRECTION ( 'NONE',  ( 0.000000000000000000, 0.000000000000000000, 1.000000000000000000 ) ) ;
#3566=EDGE_CURVE ( 'NONE', #20478, #2569, #12575, .T. ) ;
#3586=CARTESIAN_POINT ( 'NONE',  ( 42.30949999999999989, 0.000000000000000000, 0.000000000000000000 ) ) ;
#3630=( GEOMETRIC_REPRESENTATION_CONTEXT ( 3 ) GLOBAL_UNCERTAINTY_ASSIGNED_CONTEXT ( ( #3211 ) ) GLOBAL_UNIT_ASSIGNED_CONTEXT ( ( #2630, #19149, #10990 ) ) REPRESENTATION_CONTEXT ( 'NONE', 'WORKASPACE' ) );
#3694=CARTESIAN_POINT ( 'NONE',  ( 7.999999999999998224, 6.500000000000000000, 0.000000000000000000 ) ) ;
#3709=DIRECTION ( 'NONE',  ( -1.000000000000000000, -0.000000000000000000, -0.000000000000000000 ) ) ;
#3759=ADVANCED_BREP_SHAPE_REPRESENTATION ( '', ( #17281, #18233 ), #2321 ) ;
#3795=PRODUCT_DEFINITION ( 'UNKNOWN', '', #19579, #17430 ) ;
#3806=ADVANCED_FACE ( 'NONE', ( #7436 ), #10494, .T. ) ;
#3809=DIRECTION ( 'NONE',  ( 0.000000000000000000, 0.000000000000000000, -1.000000000000000000 ) ) ;
#3821=DIRECTION ( 'NONE',  ( 0.000000000000000000, 1.000000000000000000, -1.355657144061424088E-15 ) ) ;
#3824=ORIENTED_EDGE ( 'NONE', *, *, #13923, .F. ) ;
#3921=DIRECTION ( 'NONE',  ( -0.5000000000000061062, 0.000000000000000000, 0.8660254037844351549 ) ) ;
#4047=EDGE_LOOP ( 'NONE', ( #20065, #4159, #14350 ) ) ;
#4098=CARTESIAN_POINT ( 'NONE',  ( 0.000000000000000000, -1.759474945355379072, 3.047500000000001652 ) ) ;
#4111=DIRECTION ( 'NONE',  ( 0.000000000000000000, 0.000000000000000000, 1.000000000000000000 ) ) ;
#4154=CARTESIAN_POINT ( 'NONE',  ( 8.000000000000000000, 7.960204194457795477E-16, -6.500000000000000000 ) ) ;
#4159=ORIENTED_EDGE ( 'NONE', *, *, #3215, .T. ) ;
#4181=CARTESIAN_POINT ( 'NONE',  ( 4.000000000000000000, -1.759474945355379072, 3.047500000000001652 ) ) ;
#4204=DIRECTION ( 'NONE',  ( 0.000000000000000000, 0.000000000000000000, 1.000000000000000000 ) ) ;
#4218=AXIS2_PLACEMENT_3D ( 'NONE', #45, #146, #17539 ) ;
#4264=VECTOR ( 'NONE', #8528, 999.9999999999998863 ) ;
#4278=AXIS2_PLACEMENT_3D ( 'NONE', #15100, #7115, #13604 ) ;
#4280=CARTESIAN_POINT ( 'NONE',  ( 4.000000000000000000, -3.518949890710766581, 4.553649124439118623E-15 ) ) ;
#4284=CARTESIAN_POINT ( 'NONE',  ( 0.3999999999999975797, 7.960204194457795477E-16, -6.500000000000000000 ) ) ;
#4322=LINE ( 'NONE', #7598, #12540 ) ;
#4458=APPLICATION_CONTEXT ( 'automotive_design' ) ;
#4462=PLANE ( 'NONE',  #18357 ) ;
#4519=ORIENTED_EDGE ( 'NONE', *, *, #2033, .F. ) ;
#4552=ORIENTED_EDGE ( 'NONE', *, *, #9413, .T. ) ;
#4556=EDGE_CURVE ( 'NONE', #7000, #5435, #8653, .T. ) ;
#4612=DIRECTION ( 'NONE',  ( 1.000000000000000000, 0.000000000000000000, 0.000000000000000000 ) ) ;
#4638=ORIENTED_EDGE ( 'NONE', *, *, #376, .F. ) ;
#4668=AXIS2_PLACEMENT_3D ( 'NONE', #5861, #15753, #14055 ) ;
#4710=CARTESIAN_POINT ( 'NONE',  ( 4.000000000000000000, -1.759474945355379072, 3.047500000000001652 ) ) ;
#4736=ORIENTED_EDGE ( 'NONE', *, *, #8893, .F. ) ;
#4868=DIRECTION ( 'NONE',  ( -1.000000000000000000, -0.000000000000000000, -0.000000000000000000 ) ) ;
#4877=CARTESIAN_POINT ( 'NONE',  ( 4.000000000000000000, 3.518949890710767026, -4.987329993433320396E-15 ) ) ;
#4900=ORIENTED_EDGE ( 'NONE', *, *, #10765, .T. ) ;
#4918=CIRCLE ( 'NONE', #11363, 3.047499999999999876 ) ;
#4940=EDGE_LOOP ( 'NONE', ( #13072, #790, #9800, #18970, #1604 ) ) ;
#4969=VERTEX_POINT ( 'NONE', #4154 ) ;
#5003=CARTESIAN_POINT ( 'NONE',  ( 4.000000000000000000, -3.518949890710766581, 4.553649124439118623E-15 ) ) ;
#5070=ORIENTED_EDGE ( 'NONE', *, *, #10706, .T. ) ;
#5088=PLANE ( 'NONE',  #11301 ) ;
#5103=DIRECTION ( 'NONE',  ( -1.000000000000000000, -0.000000000000000000, -0.000000000000000000 ) ) ;
#5106=PLANE ( 'NONE',  #9300 ) ;
#5128=CARTESIAN_POINT ( 'NONE',  ( 43.00000000000000000, 0.000000000000000000, 3.309499999999999886 ) ) ;
#5167=ORIENTED_EDGE ( 'NONE', *, *, #14381, .T. ) ;
#5241=DIRECTION ( 'NONE',  ( -1.000000000000000000, -0.000000000000000000, -0.000000000000000000 ) ) ;
#5269=ORIENTED_EDGE ( 'NONE', *, *, #9400, .F. ) ;
#5272=ORIENTED_EDGE ( 'NONE', *, *, #15628, .F. ) ;
#5292=ORIENTED_EDGE ( 'NONE', *, *, #833, .F. ) ;
#5301=VECTOR ( 'NONE', #2871, 1000.000000000000000 ) ;
#5322=ORIENTED_EDGE ( 'NONE', *, *, #2048, .F. ) ;
#5361=AXIS2_PLACEMENT_3D ( 'NONE', #18131, #10153, #13473 ) ;
#5435=VERTEX_POINT ( 'NONE', #20640 ) ;
#5461=ORIENTED_EDGE ( 'NONE', *, *, #16804, .F. ) ;
#5468=ADVANCED_FACE ( 'NONE', ( #2751 ), #17289, .F. ) ;
#5505=CARTESIAN_POINT ( 'NONE',  ( 4.000000000000000000, -3.755786496842899057E-15, -3.047499999999999876 ) ) ;
#5509=ORIENTED_EDGE ( 'NONE', *, *, #8242, .T. ) ;
#5670=DIRECTION ( 'NONE',  ( 0.000000000000000000, -0.5000000000000008882, -0.8660254037844380415 ) ) ;
#5671=CIRCLE ( 'NONE', #15200, 6.099999999999999645 ) ;
#5763=AXIS2_PLACEMENT_3D ( 'NONE', #6220, #18960, #20440 ) ;
#5780=VECTOR ( 'NONE', #14933, 1000.000000000000114 ) ;
#5861=CARTESIAN_POINT ( 'NONE',  ( 0.3999999999999975797, 0.000000000000000000, 0.000000000000000000 ) ) ;
#5898=EDGE_LOOP ( 'NONE', ( #19191, #19908, #12731, #8617 ) ) ;
#6016=CARTESIAN_POINT ( 'NONE',  ( 4.000000000000000000, -3.518949890710766581, 4.553649124439118623E-15 ) ) ;
#6162=CIRCLE ( 'NONE', #7861, 3.047499999999999876 ) ;
#6177=ADVANCED_FACE ( 'NONE', ( #18904 ), #10829, .F. ) ;
#6220=CARTESIAN_POINT ( 'NONE',  ( 8.399999999999998579, 0.000000000000000000, 0.000000000000000000 ) ) ;
#6225=DIRECTION ( 'NONE',  ( 0.000000000000000000, 0.4999999999999985012, -0.8660254037844394848 ) ) ;
#6230=SHAPE_REPRESENTATION ( 'socket head cap screw_iso_ISO 4762 M8 x 35 - 35N', ( #18233 ), #2321 ) ;
#6236=DIRECTION ( 'NONE',  ( 0.000000000000000000, 0.000000000000000000, 1.000000000000000000 ) ) ;
#6280=EDGE_CURVE ( 'NONE', #6599, #6373, #16238, .T. ) ;
#6301=LINE ( 'NONE', #261, #6612 ) ;
#6307=DIRECTION ( 'NONE',  ( 0.000000000000000000, 1.000000000000000000, -1.355657144061424088E-15 ) ) ;
#6315=CARTESIAN_POINT ( 'NONE',  ( 4.000000000000000000, 0.000000000000000000, 0.000000000000000000 ) ) ;
#6319=AXIS2_PLACEMENT_3D ( 'NONE', #19282, #11228, #17697 ) ;
#6330=CIRCLE ( 'NONE', #4668, 6.500000000000000000 ) ;
#6355=CARTESIAN_POINT ( 'NONE',  ( 0.000000000000000000, -1.759474945355379072, 3.047500000000001652 ) ) ;
#6357=DIRECTION ( 'NONE',  ( 0.000000000000000000, 0.4999999999999985567, -0.8660254037844393737 ) ) ;
#6373=VERTEX_POINT ( 'NONE', #2455 ) ;
#6399=CARTESIAN_POINT ( 'NONE',  ( 8.000000000000000000, 0.000000000000000000, 6.500000000000000000 ) ) ;
#6451=AXIS2_PLACEMENT_3D ( 'NONE', #3435, #256, #17761 ) ;
#6456=PLANE ( 'NONE',  #8487 ) ;
#6460=AXIS2_PLACEMENT_3D ( 'NONE', #7685, #921, #4204 ) ;
#6535=ADVANCED_FACE ( 'NONE', ( #14016 ), #4462, .F. ) ;
#6543=DIRECTION ( 'NONE',  ( 0.000000000000000000, 0.4999999999999985012, -0.8660254037844394848 ) ) ;
#6576=ORIENTED_EDGE ( 'NONE', *, *, #10362, .F. ) ;
#6589=FACE_OUTER_BOUND ( 'NONE', #13633, .T. ) ;
#6599=VERTEX_POINT ( 'NONE', #8643 ) ;
#6604=DIRECTION ( 'NONE',  ( 0.000000000000000000, 0.000000000000000000, 1.000000000000000000 ) ) ;
#6612=VECTOR ( 'NONE', #9791, 1000.000000000000000 ) ;
#6613=DIRECTION ( 'NONE',  ( 0.000000000000000000, -0.4999999999999985567, 0.8660254037844393737 ) ) ;
#6621=CARTESIAN_POINT ( 'NONE',  ( 43.00000000000000000, 0.000000000000000000, 0.000000000000000000 ) ) ;
#6690=DIRECTION ( 'NONE',  ( -1.000000000000000000, -0.000000000000000000, -0.000000000000000000 ) ) ;
#6719=DIRECTION ( 'NONE',  ( -1.000000000000000000, -0.000000000000000000, -0.000000000000000000 ) ) ;
#6763=VECTOR ( 'NONE', #129, 1000.000000000000000 ) ;
#6776=LINE ( 'NONE', #331, #6763 ) ;
#6782=EDGE_CURVE ( 'NONE', #11275, #1811, #18188, .T. ) ;
#6891=CARTESIAN_POINT ( 'NONE',  ( 4.000000000000000000, 3.518949890710767026, -4.987329993433320396E-15 ) ) ;
#6900=ORIENTED_EDGE ( 'NONE', *, *, #13935, .T. ) ;
#6904=CARTESIAN_POINT ( 'NONE',  ( 8.000000000000000000, 0.000000000000000000, 0.000000000000000000 ) ) ;
#6941=LINE ( 'NONE', #8645, #2603 ) ;
#7000=VERTEX_POINT ( 'NONE', #16048 ) ;
#7047=EDGE_CURVE ( 'NONE', #1811, #20230, #6776, .T. ) ;
#7094=FACE_OUTER_BOUND ( 'NONE', #15389, .T. ) ;
#7115=DIRECTION ( 'NONE',  ( -1.000000000000000000, -0.000000000000000000, -0.000000000000000000 ) ) ;
#7158=ORIENTED_EDGE ( 'NONE', *, *, #2033, .T. ) ;
#7201=CARTESIAN_POINT ( 'NONE',  ( 0.000000000000000000, -1.759474945355387954, -3.047499999999997211 ) ) ;
#7221=EDGE_CURVE ( 'NONE', #14920, #17008, #5671, .T. ) ;
#7292=VERTEX_POINT ( 'NONE', #5505 ) ;
#7293=CIRCLE ( 'NONE', #17811, 6.500000000000000000 ) ;
#7303=CARTESIAN_POINT ( 'NONE',  ( 4.000000000000000000, -1.759474945355379072, 3.047500000000001652 ) ) ;
#7334=DIRECTION ( 'NONE',  ( 0.000000000000000000, 0.000000000000000000, 1.000000000000000000 ) ) ;
#7406=EDGE_CURVE ( 'NONE', #15178, #7292, #12724, .T. ) ;
#7436=FACE_OUTER_BOUND ( 'NONE', #5898, .T. ) ;
#7515=EDGE_CURVE ( 'NONE', #7969, #6373, #9448, .T. ) ;
#7598=CARTESIAN_POINT ( 'NONE',  ( 0.000000000000000000, 3.518949890710767026, -4.987329993433320396E-15 ) ) ;
#7655=LINE ( 'NONE', #20381, #2747 ) ;
#7685=CARTESIAN_POINT ( 'NONE',  ( -31.74999999999995737, 0.000000000000000000, 0.000000000000000000 ) ) ;
#7689=AXIS2_PLACEMENT_3D ( 'NONE', #16852, #8896, #18552 ) ;
#7704=ORIENTED_EDGE ( 'NONE', *, *, #10765, .F. ) ;
#7724=CARTESIAN_POINT ( 'NONE',  ( 8.399999999999998579, 0.000000000000000000, 4.000000000000000000 ) ) ;
#7754=CARTESIAN_POINT ( 'NONE',  ( 4.000000000000000000, 5.278424836066145431, -3.047500000000006093 ) ) ;
#7768=FACE_OUTER_BOUND ( 'NONE', #13859, .T. ) ;
#7797=VECTOR ( 'NONE', #18909, 1000.000000000000000 ) ;
#7798=EDGE_CURVE ( 'NONE', #1811, #15672, #4322, .T. ) ;
#7861=AXIS2_PLACEMENT_3D ( 'NONE', #12066, #2419, #4111 ) ;
#7969=VERTEX_POINT ( 'NONE', #13327 ) ;
#7982=DIRECTION ( 'NONE',  ( 0.000000000000000000, -1.232415585510385534E-15, -1.000000000000000000 ) ) ;
#7985=DIRECTION ( 'NONE',  ( -1.000000000000000000, -0.000000000000000000, -0.000000000000000000 ) ) ;
#7996=DIRECTION ( 'NONE',  ( -1.000000000000000000, -0.000000000000000000, -0.000000000000000000 ) ) ;
#8019=ORIENTED_EDGE ( 'NONE', *, *, #475, .T. ) ;
#8049=FACE_OUTER_BOUND ( 'NONE', #559, .T. ) ;
#8075=DIRECTION ( 'NONE',  ( 0.000000000000000000, -1.224646799147353207E-16, 1.000000000000000000 ) ) ;
#8090=CARTESIAN_POINT ( 'NONE',  ( -31.74999999999995737, 0.000000000000000000, 0.000000000000000000 ) ) ;
#8124=ORIENTED_EDGE ( 'NONE', *, *, #763, .F. ) ;
#8186=CARTESIAN_POINT ( 'NONE',  ( -31.74999999999995737, 0.000000000000000000, 4.000000000000000000 ) ) ;
#8216=CARTESIAN_POINT ( 'NONE',  ( -31.74999999999995737, 0.000000000000000000, 0.000000000000000000 ) ) ;
#8228=FACE_OUTER_BOUND ( 'NONE', #18540, .T. ) ;
#8229=AXIS2_PLACEMENT_3D ( 'NONE', #8320, #6719, #3554 ) ;
#8233=EDGE_CURVE ( 'NONE', #140, #7292, #14286, .T. ) ;
#8242=EDGE_CURVE ( 'NONE', #11211, #18235, #14268, .T. ) ;
#8254=FACE_BOUND ( 'NONE', #20644, .T. ) ;
#8283=DIRECTION ( 'NONE',  ( 1.000000000000000000, 0.000000000000000000, 0.000000000000000000 ) ) ;
#8316=AXIS2_PLACEMENT_3D ( 'NONE', #17791, #3263, #9715 ) ;
#8320=CARTESIAN_POINT ( 'NONE',  ( 4.000000000000000000, 0.000000000000000000, 0.000000000000000000 ) ) ;
#8390=ORIENTED_EDGE ( 'NONE', *, *, #9413, .F. ) ;
#8426=DIRECTION ( 'NONE',  ( 0.000000000000000000, 0.000000000000000000, 1.000000000000000000 ) ) ;
#8442=CARTESIAN_POINT ( 'NONE',  ( -31.74999999999995737, 0.000000000000000000, 0.000000000000000000 ) ) ;
#8459=ORIENTED_EDGE ( 'NONE', *, *, #15118, .T. ) ;
#8482=ORIENTED_EDGE ( 'NONE', *, *, #14081, .F. ) ;
#8485=VECTOR ( 'NONE', #18400, 1000.000000000000000 ) ;
#8487=AXIS2_PLACEMENT_3D ( 'NONE', #1505, #20881, #6357 ) ;
#8528=DIRECTION ( 'NONE',  ( -0.7071067811865462405, 0.000000000000000000, 0.7071067811865489050 ) ) ;
#8559=ORIENTED_EDGE ( 'NONE', *, *, #9400, .T. ) ;
#8617=ORIENTED_EDGE ( 'NONE', *, *, #9622, .F. ) ;
#8635=EDGE_LOOP ( 'NONE', ( #8482, #5461, #1600, #1660 ) ) ;
#8643=CARTESIAN_POINT ( 'NONE',  ( 43.00000000000000000, 4.475777889183787821E-16, -3.309499999999999886 ) ) ;
#8645=CARTESIAN_POINT ( 'NONE',  ( -31.74999999999995737, 7.960204194457795477E-16, -6.500000000000000000 ) ) ;
#8647=ORIENTED_EDGE ( 'NONE', *, *, #19344, .F. ) ;
#8653=LINE ( 'NONE', #13540, #5780 ) ;
#8673=DIRECTION ( 'NONE',  ( 0.000000000000000000, 1.000000000000000000, -1.224646799147353207E-16 ) ) ;
#8696=CARTESIAN_POINT ( 'NONE',  ( 0.000000000000000000, -1.759474945355379072, 3.047500000000001652 ) ) ;
#8700=EDGE_CURVE ( 'NONE', #15178, #20230, #20481, .T. ) ;
#8708=DIRECTION ( 'NONE',  ( 0.000000000000000000, 0.000000000000000000, 1.000000000000000000 ) ) ;
#8743=EDGE_CURVE ( 'NONE', #12993, #1364, #7655, .T. ) ;
#8760=EDGE_LOOP ( 'NONE', ( #7704, #14983, #18051, #5070, #14259 ) ) ;
#8761=DIRECTION ( 'NONE',  ( 0.000000000000000000, -0.5000000000000008882, -0.8660254037844380415 ) ) ;
#8892=VECTOR ( 'NONE', #5670, 1000.000000000000227 ) ;
#8893=EDGE_CURVE ( 'NONE', #20230, #1364, #16000, .T. ) ;
#8896=DIRECTION ( 'NONE',  ( 1.000000000000000000, 0.000000000000000000, 0.000000000000000000 ) ) ;
#8907=CARTESIAN_POINT ( 'NONE',  ( 0.000000000000000000, 0.000000000000000000, 0.000000000000000000 ) ) ;
#8934=LINE ( 'NONE', #676, #14956 ) ;
#9008=EDGE_CURVE ( 'NONE', #12336, #7292, #2061, .T. ) ;
#9040=ORIENTED_EDGE ( 'NONE', *, *, #6782, .F. ) ;
#9094=ORIENTED_EDGE ( 'NONE', *, *, #4556, .F. ) ;
#9149=CARTESIAN_POINT ( 'NONE',  ( 0.000000000000000000, 3.518949890710767026, -4.987329993433320396E-15 ) ) ;
#9158=CARTESIAN_POINT ( 'NONE',  ( 4.000000000000000000, 3.732111120401558708E-16, -3.047499999999999876 ) ) ;
#9255=SHAPE_REPRESENTATION_RELATIONSHIP ( 'NONE' , 'NONE' ,  #6230, #3759 ) ;
#9261=DIRECTION ( 'NONE',  ( 0.000000000000000000, -0.5000000000000008882, -0.8660254037844380415 ) ) ;
#9265=DIRECTION ( 'NONE',  ( 1.000000000000000000, 0.000000000000000000, 0.000000000000000000 ) ) ;
#9291=ORIENTED_EDGE ( 'NONE', *, *, #14081, .T. ) ;
#9300=AXIS2_PLACEMENT_3D ( 'NONE', #11798, #8283, #11591 ) ;
#9367=DIRECTION ( 'NONE',  ( 0.000000000000000000, 0.000000000000000000, -1.000000000000000000 ) ) ;
#9400=EDGE_CURVE ( 'NONE', #18781, #3452, #13260, .T. ) ;
#9413=EDGE_CURVE ( 'NONE', #15824, #20638, #10874, .T. ) ;
#9448=CIRCLE ( 'NONE', #19288, 3.999999999999999112 ) ;
#9464=ADVANCED_FACE ( 'NONE', ( #16269 ), #11394, .F. ) ;
#9486=EDGE_LOOP ( 'NONE', ( #8647, #13117, #8124 ) ) ;
#9573=CARTESIAN_POINT ( 'NONE',  ( 4.000000000000000000, 1.759474945355379960, -3.047500000000001652 ) ) ;
#9608=ORIENTED_EDGE ( 'NONE', *, *, #8743, .T. ) ;
#9622=EDGE_CURVE ( 'NONE', #18235, #17008, #2078, .T. ) ;
#9637=EDGE_CURVE ( 'NONE', #5435, #15672, #8934, .T. ) ;
#9684=AXIS2_PLACEMENT_3D ( 'NONE', #8216, #3460, #2088 ) ;
#9689=CYLINDRICAL_SURFACE ( 'NONE', #241, 4.000000000000000000 ) ;
#9715=DIRECTION ( 'NONE',  ( 0.000000000000000000, 0.000000000000000000, -1.000000000000000000 ) ) ;
#9791=DIRECTION ( 'NONE',  ( 0.000000000000000000, -1.000000000000000000, 1.232415585510385534E-15 ) ) ;
#9800=ORIENTED_EDGE ( 'NONE', *, *, #16117, .F. ) ;
#9810=ORIENTED_EDGE ( 'NONE', *, *, #10362, .T. ) ;
#9820=CARTESIAN_POINT ( 'NONE',  ( 0.000000000000000000, 0.000000000000000000, 6.099999999999999645 ) ) ;
#9922=ADVANCED_FACE ( 'NONE', ( #10477 ), #12315, .T. ) ;
#9924=ORIENTED_EDGE ( 'NONE', *, *, #376, .T. ) ;
#9985=CARTESIAN_POINT ( 'NONE',  ( 4.000000000000000000, 3.518949890710767026, -4.987329993433320396E-15 ) ) ;
#10000=VECTOR ( 'NONE', #1590, 1000.000000000000000 ) ;
#10135=DIRECTION ( 'NONE',  ( 0.000000000000000000, 1.224646799147353207E-16, 1.000000000000000000 ) ) ;
#10144=CARTESIAN_POINT ( 'NONE',  ( 8.000000000000000000, 0.000000000000000000, 0.000000000000000000 ) ) ;
#10148=DIRECTION ( 'NONE',  ( 1.000000000000000000, 0.000000000000000000, 0.000000000000000000 ) ) ;
#10153=DIRECTION ( 'NONE',  ( 1.000000000000000000, 0.000000000000000000, 0.000000000000000000 ) ) ;
#10255=DIRECTION ( 'NONE',  ( 0.000000000000000000, 0.000000000000000000, 1.000000000000000000 ) ) ;
#10263=CONICAL_SURFACE ( 'NONE', #15054, 3.047499999999999876, 1.047197551196590748 ) ;
#10289=DIRECTION ( 'NONE',  ( 0.000000000000000000, 0.000000000000000000, -1.000000000000000000 ) ) ;
#10362=EDGE_CURVE ( 'NONE', #17399, #2569, #6162, .T. ) ;
#10377=CARTESIAN_POINT ( 'NONE',  ( 4.000000000000000000, 0.000000000000000000, 0.000000000000000000 ) ) ;
#10392=CARTESIAN_POINT ( 'NONE',  ( 4.000000000000000000, 5.278424836066145431, -3.047500000000006093 ) ) ;
#10477=FACE_OUTER_BOUND ( 'NONE', #8760, .T. ) ;
#10494=TOROIDAL_SURFACE ( 'NONE', #2042, 6.099999999999999645, 0.4000000000000000222 ) ;
#10624=CARTESIAN_POINT ( 'NONE',  ( 4.000000000000000000, -1.759474945355379072, 3.047500000000001652 ) ) ;
#10649=CIRCLE ( 'NONE', #11729, 3.309499999999999886 ) ;
#10696=AXIS2_PLACEMENT_3D ( 'NONE', #2253, #5103, #8708 ) ;
#10706=EDGE_CURVE ( 'NONE', #2569, #18021, #2406, .T. ) ;
#10753=ORIENTED_EDGE ( 'NONE', *, *, #9622, .T. ) ;
#10765=EDGE_CURVE ( 'NONE', #18457, #17954, #16925, .T. ) ;
#10829=PLANE ( 'NONE',  #16964 ) ;
#10843=UNCERTAINTY_MEASURE_WITH_UNIT (LENGTH_MEASURE( 1.000000000000000082E-05 ), #20398, 'distance_accuracy_value', 'NONE');
#10854=( NAMED_UNIT ( * ) SI_UNIT ( $, .STERADIAN. ) SOLID_ANGLE_UNIT ( ) );
#10874=CIRCLE ( 'NONE', #17655, 4.400000000000000355 ) ;
#10939=VECTOR ( 'NONE', #16324, 1000.000000000000000 ) ;
#10957=VECTOR ( 'NONE', #6307, 1000.000000000000000 ) ;
#10971=( NAMED_UNIT ( * ) PLANE_ANGLE_UNIT ( ) SI_UNIT ( $, .RADIAN. ) );
#10990=( NAMED_UNIT ( * ) SI_UNIT ( $, .STERADIAN. ) SOLID_ANGLE_UNIT ( ) );
#11059=CONICAL_SURFACE ( 'NONE', #17496, 3.309499999999999886, 0.7853981633974501664 ) ;
#11082=EDGE_LOOP ( 'NONE', ( #11837, #3264, #14971, #14342, #19068 ) ) ;
#11197=VECTOR ( 'NONE', #20744, 1000.000000000000000 ) ;
#11211=VERTEX_POINT ( 'NONE', #4284 ) ;
#11228=DIRECTION ( 'NONE',  ( 0.000000000000000000, -1.000000000000000000, 0.000000000000000000 ) ) ;
#11275=VERTEX_POINT ( 'NONE', #4877 ) ;
#11301=AXIS2_PLACEMENT_3D ( 'NONE', #17836, #28, #19412 ) ;
#11363=AXIS2_PLACEMENT_3D ( 'NONE', #20652, #73, #2967 ) ;
#11394=PLANE ( 'NONE',  #6451 ) ;
#11429=DIRECTION ( 'NONE',  ( 0.000000000000000000, 0.000000000000000000, 1.000000000000000000 ) ) ;
#11440=DIRECTION ( 'NONE',  ( -1.000000000000000000, -0.000000000000000000, -0.000000000000000000 ) ) ;
#11506=CARTESIAN_POINT ( 'NONE',  ( 4.000000000000000000, 3.518949890710767026, -4.987329993433320396E-15 ) ) ;
#11531=DIRECTION ( 'NONE',  ( -1.000000000000000000, -0.000000000000000000, -0.000000000000000000 ) ) ;
#11580=ORIENTED_EDGE ( 'NONE', *, *, #14163, .T. ) ;
#11591=DIRECTION ( 'NONE',  ( 0.000000000000000000, 0.000000000000000000, -1.000000000000000000 ) ) ;
#11643=CIRCLE ( 'NONE', #8229, 3.047499999999999876 ) ;
#11669=FACE_OUTER_BOUND ( 'NONE', #16669, .T. ) ;
#11729=AXIS2_PLACEMENT_3D ( 'NONE', #6621, #13218, #8426 ) ;
#11739=ADVANCED_FACE ( 'NONE', ( #6589 ), #14694, .F. ) ;
#11756=DIRECTION ( 'NONE',  ( 0.000000000000000000, 0.000000000000000000, 1.000000000000000000 ) ) ;
#11770=FACE_OUTER_BOUND ( 'NONE', #2122, .T. ) ;
#11782=DIRECTION ( 'NONE',  ( 0.000000000000000000, 0.5000000000000009992, 0.8660254037844380415 ) ) ;
#11787=AXIS2_PLACEMENT_3D ( 'NONE', #6904, #19838, #560 ) ;
#11798=CARTESIAN_POINT ( 'NONE',  ( 4.000000000000000000, 5.278424836066145431, -3.047500000000006093 ) ) ;
#11809=CARTESIAN_POINT ( 'NONE',  ( 0.3999999999999975797, 0.000000000000000000, 6.099999999999999645 ) ) ;
#11837=ORIENTED_EDGE ( 'NONE', *, *, #8233, .F. ) ;
#11851=VECTOR ( 'NONE', #9261, 1000.000000000000227 ) ;
#11859=CARTESIAN_POINT ( 'NONE',  ( 0.000000000000000000, -3.518949890710766581, 4.553649124439118623E-15 ) ) ;
#11878=DIRECTION ( 'NONE',  ( 1.000000000000000000, 0.000000000000000000, 0.000000000000000000 ) ) ;
#11882=DIRECTION ( 'NONE',  ( -1.000000000000000000, -0.000000000000000000, -0.000000000000000000 ) ) ;
#11916=CARTESIAN_POINT ( 'NONE',  ( 7.999999999999998224, 5.388445916248354013E-16, 4.400000000000000355 ) ) ;
#11948=CYLINDRICAL_SURFACE ( 'NONE', #9684, 6.500000000000000000 ) ;
#11949=ORIENTED_EDGE ( 'NONE', *, *, #14163, .F. ) ;
#11990=VECTOR ( 'NONE', #3821, 1000.000000000000000 ) ;
#12015=ADVANCED_FACE ( 'NONE', ( #14034 ), #3456, .F. ) ;
#12066=CARTESIAN_POINT ( 'NONE',  ( 4.000000000000000000, 0.000000000000000000, 0.000000000000000000 ) ) ;
#12196=ORIENTED_EDGE ( 'NONE', *, *, #8743, .F. ) ;
#12199=CARTESIAN_POINT ( 'NONE',  ( 4.000000000000000000, 4.131365146527188963E-15, 3.047499999999999432 ) ) ;
#12241=ORIENTED_EDGE ( 'NONE', *, *, #7406, .T. ) ;
#12275=CYLINDRICAL_SURFACE ( 'NONE', #6460, 6.500000000000000000 ) ;
#12281=ORIENTED_EDGE ( 'NONE', *, *, #14461, .T. ) ;
#12291=CARTESIAN_POINT ( 'NONE',  ( -31.74999999999995737, 4.898587196589412829E-16, -4.000000000000000000 ) ) ;
#12315=PLANE ( 'NONE',  #13277 ) ;
#12336=VERTEX_POINT ( 'NONE', #1611 ) ;
#12367=DIRECTION ( 'NONE',  ( -0.5000000000000061062, 1.060575238724902601E-16, -0.8660254037844351549 ) ) ;
#12411=ORIENTED_EDGE ( 'NONE', *, *, #1923, .T. ) ;
#12414=CIRCLE ( 'NONE', #16799, 3.999999999999999112 ) ;
#12462=EDGE_CURVE ( 'NONE', #20638, #15824, #1442, .T. ) ;
#12480=LINE ( 'NONE', #19147, #14128 ) ;
#12494=DIRECTION ( 'NONE',  ( -1.000000000000000000, -0.000000000000000000, -0.000000000000000000 ) ) ;
#12504=EDGE_CURVE ( 'NONE', #140, #12601, #20039, .T. ) ;
#12540=VECTOR ( 'NONE', #17253, 1000.000000000000114 ) ;
#12558=AXIS2_PLACEMENT_3D ( 'NONE', #20610, #4612, #12683 ) ;
#12575=LINE ( 'NONE', #4710, #11851 ) ;
#12601=VERTEX_POINT ( 'NONE', #12199 ) ;
#12640=ORIENTED_EDGE ( 'NONE', *, *, #13104, .T. ) ;
#12676=AXIS2_PLACEMENT_3D ( 'NONE', #6891, #333, #11782 ) ;
#12683=DIRECTION ( 'NONE',  ( 0.000000000000000000, 0.000000000000000000, 1.000000000000000000 ) ) ;
#12724=LINE ( 'NONE', #14014, #5301 ) ;
#12731=ORIENTED_EDGE ( 'NONE', *, *, #20148, .F. ) ;
#12757=EDGE_CURVE ( 'NONE', #17954, #1364, #20011, .T. ) ;
#12811=CARTESIAN_POINT ( 'NONE',  ( 0.000000000000000000, 1.759474945355379960, -3.047500000000001652 ) ) ;
#12873=ORIENTED_EDGE ( 'NONE', *, *, #8233, .T. ) ;
#12993=VERTEX_POINT ( 'NONE', #18638 ) ;
#13072=ORIENTED_EDGE ( 'NONE', *, *, #7047, .T. ) ;
#13089=DIRECTION ( 'NONE',  ( 0.000000000000000000, 1.000000000000000000, -1.232415585510385534E-15 ) ) ;
#13104=EDGE_CURVE ( 'NONE', #12601, #5435, #17365, .T. ) ;
#13117=ORIENTED_EDGE ( 'NONE', *, *, #3087, .T. ) ;
#13166=DIRECTION ( 'NONE',  ( -0.7071067811865462405, 8.659560562354950115E-17, -0.7071067811865489050 ) ) ;
#13206=EDGE_CURVE ( 'NONE', #2569, #12601, #11643, .T. ) ;
#13218=DIRECTION ( 'NONE',  ( -1.000000000000000000, -0.000000000000000000, -0.000000000000000000 ) ) ;
#13260=CIRCLE ( 'NONE', #1418, 4.000000000000000000 ) ;
#13277=AXIS2_PLACEMENT_3D ( 'NONE', #7303, #2449, #18560 ) ;
#13298=CARTESIAN_POINT ( 'NONE',  ( 4.000000000000000000, -1.759474945355379072, 3.047500000000001652 ) ) ;
#13299=PRODUCT_DEFINITION_SHAPE ( 'NONE', 'NONE',  #3795 ) ;
#13319=LINE ( 'NONE', #11506, #15240 ) ;
#13327=CARTESIAN_POINT ( 'NONE',  ( 42.30949999999999989, 0.000000000000000000, 3.999999999999999112 ) ) ;
#13406=ORIENTED_EDGE ( 'NONE', *, *, #17442, .F. ) ;
#13432=FACE_OUTER_BOUND ( 'NONE', #3537, .T. ) ;
#13443=ORIENTED_EDGE ( 'NONE', *, *, #17442, .T. ) ;
#13457=AXIS2_PLACEMENT_3D ( 'NONE', #8442, #11531, #11429 ) ;
#13473=DIRECTION ( 'NONE',  ( 0.000000000000000000, 0.000000000000000000, -1.000000000000000000 ) ) ;
#13500=DIRECTION ( 'NONE',  ( 1.000000000000000000, 0.000000000000000000, 0.000000000000000000 ) ) ;
#13528=CARTESIAN_POINT ( 'NONE',  ( 4.000000000000000000, 3.518949890710767026, -4.987329993433320396E-15 ) ) ;
#13535=ADVANCED_FACE ( 'NONE', ( #19610 ), #5088, .F. ) ;
#13540=CARTESIAN_POINT ( 'NONE',  ( 4.000000000000000000, 3.518949890710767026, -4.987329993433320396E-15 ) ) ;
#13550=AXIS2_PLACEMENT_3D ( 'NONE', #10392, #13500, #10289 ) ;
#13556=EDGE_CURVE ( 'NONE', #18457, #15672, #16443, .T. ) ;
#13581=PLANE ( 'NONE',  #5361 ) ;
#13589=DIRECTION ( 'NONE',  ( 0.000000000000000000, 0.000000000000000000, 1.000000000000000000 ) ) ;
#13590=FACE_OUTER_BOUND ( 'NONE', #4940, .T. ) ;
#13593=ADVANCED_FACE ( 'NONE', ( #647 ), #10263, .F. ) ;
#13604=DIRECTION ( 'NONE',  ( 0.000000000000000000, 0.000000000000000000, 1.000000000000000000 ) ) ;
#13623=ORIENTED_EDGE ( 'NONE', *, *, #1986, .F. ) ;
#13633=EDGE_LOOP ( 'NONE', ( #15132, #12196, #4638, #16580, #602 ) ) ;
#13650=ADVANCED_FACE ( 'NONE', ( #13590 ), #18137, .F. ) ;
#13677=DIRECTION ( 'NONE',  ( -1.000000000000000000, -0.000000000000000000, -0.000000000000000000 ) ) ;
#13720=DIRECTION ( 'NONE',  ( 0.000000000000000000, -1.000000000000000000, 0.000000000000000000 ) ) ;
#13806=VECTOR ( 'NONE', #6225, 1000.000000000000000 ) ;
#13821=PRODUCT ( 'socket head cap screw_iso_ISO 4762 M8 x 35 - 35N', 'socket head cap screw_iso_ISO 4762 M8 x 35 - 35N', '', ( #17403 ) ) ;
#13830=ORIENTED_EDGE ( 'NONE', *, *, #4556, .T. ) ;
#13859=EDGE_LOOP ( 'NONE', ( #5167, #2117, #71, #2097 ) ) ;
#13867=ORIENTED_EDGE ( 'NONE', *, *, #13958, .T. ) ;
#13923=EDGE_CURVE ( 'NONE', #423, #18235, #111, .T. ) ;
#13934=AXIS2_PLACEMENT_3D ( 'NONE', #11809, #13720, #16578 ) ;
#13935=EDGE_CURVE ( 'NONE', #17399, #12993, #16216, .T. ) ;
#13958=EDGE_CURVE ( 'NONE', #6373, #7969, #12414, .T. ) ;
#13974=FACE_OUTER_BOUND ( 'NONE', #19325, .T. ) ;
#14014=CARTESIAN_POINT ( 'NONE',  ( 4.000000000000000000, 1.759474945355379960, -3.047500000000001652 ) ) ;
#14016=FACE_OUTER_BOUND ( 'NONE', #9486, .T. ) ;
#14034=FACE_OUTER_BOUND ( 'NONE', #2151, .T. ) ;
#14055=DIRECTION ( 'NONE',  ( 0.000000000000000000, 0.000000000000000000, 1.000000000000000000 ) ) ;
#14081=EDGE_CURVE ( 'NONE', #18781, #20638, #213, .T. ) ;
#14128=VECTOR ( 'NONE', #2728, 1000.000000000000000 ) ;
#14163=EDGE_CURVE ( 'NONE', #6373, #3452, #15379, .T. ) ;
#14165=CARTESIAN_POINT ( 'NONE',  ( 43.00000000000000000, 0.000000000000000000, 3.309499999999999886 ) ) ;
#14167=STYLED_ITEM('',(#20995),#17281);
#14182=ORIENTED_EDGE ( 'NONE', *, *, #14461, .F. ) ;
#14245=ORIENTED_EDGE ( 'NONE', *, *, #10706, .F. ) ;
#14252=EDGE_LOOP ( 'NONE', ( #326, #12241, #20875 ) ) ;
#14259=ORIENTED_EDGE ( 'NONE', *, *, #1986, .T. ) ;
#14268=CIRCLE ( 'NONE', #12558, 6.500000000000000000 ) ;
#14286=LINE ( 'NONE', #9158, #14919 ) ;
#14319=FACE_OUTER_BOUND ( 'NONE', #15007, .T. ) ;
#14325=AXIS2_PLACEMENT_3D ( 'NONE', #18240, #3505, #15088 ) ;
#14342=ORIENTED_EDGE ( 'NONE', *, *, #763, .T. ) ;
#14348=ADVANCED_FACE ( 'NONE', ( #13432 ), #11948, .T. ) ;
#14350=ORIENTED_EDGE ( 'NONE', *, *, #13206, .F. ) ;
#14381=EDGE_CURVE ( 'NONE', #17447, #6599, #10649, .T. ) ;
#14396=FACE_OUTER_BOUND ( 'NONE', #14997, .T. ) ;
#14414=EDGE_LOOP ( 'NONE', ( #2228, #3463, #4900, #14493, #4736, #18866 ) ) ;
#14440=ORIENTED_EDGE ( 'NONE', *, *, #7515, .T. ) ;
#14445=AXIS2_PLACEMENT_3D ( 'NONE', #1903, #8673, #10135 ) ;
#14461=EDGE_CURVE ( 'NONE', #4969, #11211, #6941, .T. ) ;
#14493=ORIENTED_EDGE ( 'NONE', *, *, #12757, .T. ) ;
#14575=ORIENTED_EDGE ( 'NONE', *, *, #16947, .F. ) ;
#14612=ADVANCED_FACE ( 'NONE', ( #18160 ), #5106, .F. ) ;
#14636=PLANE ( 'NONE',  #16810 ) ;
#14691=LINE ( 'NONE', #5003, #15412 ) ;
#14694=PLANE ( 'NONE',  #81 ) ;
#14760=TOROIDAL_SURFACE ( 'NONE', #20149, 6.099999999999999645, 0.4000000000000000222 ) ;
#14919=VECTOR ( 'NONE', #12367, 1000.000000000000000 ) ;
#14920=VERTEX_POINT ( 'NONE', #19208 ) ;
#14933=DIRECTION ( 'NONE',  ( 0.000000000000000000, -0.4999999999999985567, 0.8660254037844393737 ) ) ;
#14956=VECTOR ( 'NONE', #15119, 1000.000000000000000 ) ;
#14971=ORIENTED_EDGE ( 'NONE', *, *, #833, .T. ) ;
#14983=ORIENTED_EDGE ( 'NONE', *, *, #17981, .F. ) ;
#14986=DIRECTION ( 'NONE',  ( 0.000000000000000000, 0.000000000000000000, 1.000000000000000000 ) ) ;
#14991=ADVANCED_FACE ( 'NONE', ( #15188 ), #14760, .T. ) ;
#14997=EDGE_LOOP ( 'NONE', ( #14440, #11580, #1109, #19986 ) ) ;
#15007=EDGE_LOOP ( 'NONE', ( #16547, #13623, #16950, #6900, #9608 ) ) ;
#15050=CARTESIAN_POINT ( 'NONE',  ( 4.000000000000000000, -1.759474945355379072, 3.047500000000001652 ) ) ;
#15054=AXIS2_PLACEMENT_3D ( 'NONE', #10377, #3709, #14986 ) ;
#15076=ADVANCED_FACE ( 'NONE', ( #15083 ), #20821, .T. ) ;
#15083=FACE_OUTER_BOUND ( 'NONE', #2534, .T. ) ;
#15088=DIRECTION ( 'NONE',  ( 0.000000000000000000, 0.000000000000000000, -1.000000000000000000 ) ) ;
#15100=CARTESIAN_POINT ( 'NONE',  ( 4.000000000000000000, 0.000000000000000000, 0.000000000000000000 ) ) ;
#15118=EDGE_CURVE ( 'NONE', #7292, #17399, #4918, .T. ) ;
#15119=DIRECTION ( 'NONE',  ( -1.000000000000000000, -0.000000000000000000, -0.000000000000000000 ) ) ;
#15132=ORIENTED_EDGE ( 'NONE', *, *, #8893, .T. ) ;
#15150=ORIENTED_EDGE ( 'NONE', *, *, #17677, .T. ) ;
#15172=CIRCLE ( 'NONE', #7689, 4.000000000000000000 ) ;
#15178=VERTEX_POINT ( 'NONE', #867 ) ;
#15188=FACE_OUTER_BOUND ( 'NONE', #17524, .T. ) ;
#15200=AXIS2_PLACEMENT_3D ( 'NONE', #8907, #16972, #13589 ) ;
#15240=VECTOR ( 'NONE', #6613, 1000.000000000000114 ) ;
#15337=LINE ( 'NONE', #4181, #16296 ) ;
#15339=AXIS2_PLACEMENT_3D ( 'NONE', #2790, #17414, #2585 ) ;
#15368=CARTESIAN_POINT ( 'NONE',  ( 5.759474945355412601, 0.000000000000000000, 0.000000000000000000 ) ) ;
#15379=LINE ( 'NONE', #12291, #19825 ) ;
#15389=EDGE_LOOP ( 'NONE', ( #16793, #4519 ) ) ;
#15412=VECTOR ( 'NONE', #6690, 1000.000000000000000 ) ;
#15463=EDGE_LOOP ( 'NONE', ( #5269, #9291, #8390, #14575 ) ) ;
#15479=DIRECTION ( 'NONE',  ( -1.000000000000000000, -0.000000000000000000, -0.000000000000000000 ) ) ;
#15487=ORIENTED_EDGE ( 'NONE', *, *, #12504, .F. ) ;
#15500=CIRCLE ( 'NONE', #6319, 0.4000000000000001887 ) ;
#15540=ORIENTED_EDGE ( 'NONE', *, *, #15118, .F. ) ;
#15628=EDGE_CURVE ( 'NONE', #423, #4969, #7293, .T. ) ;
#15672=VERTEX_POINT ( 'NONE', #20849 ) ;
#15739=ORIENTED_EDGE ( 'NONE', *, *, #3215, .F. ) ;
#15748=DIRECTION ( 'NONE',  ( 0.000000000000000000, 1.000000000000000000, -1.355657144061424088E-15 ) ) ;
#15753=DIRECTION ( 'NONE',  ( 1.000000000000000000, 0.000000000000000000, 0.000000000000000000 ) ) ;
#15765=ORIENTED_EDGE ( 'NONE', *, *, #12462, .T. ) ;
#15766=CARTESIAN_POINT ( 'NONE',  ( 7.999999999999998224, 0.000000000000000000, 0.000000000000000000 ) ) ;
#15767=ADVANCED_FACE ( 'NONE', ( #14319 ), #1268, .T. ) ;
#15779=ADVANCED_FACE ( 'NONE', ( #19572, #8228 ), #14636, .T. ) ;
#15789=DIRECTION ( 'NONE',  ( 0.000000000000000000, 0.000000000000000000, 1.000000000000000000 ) ) ;
#15824=VERTEX_POINT ( 'NONE', #17694 ) ;
#15870=ADVANCED_FACE ( 'NONE', ( #1678 ), #20852, .F. ) ;
#15903=CARTESIAN_POINT ( 'NONE',  ( 0.000000000000000000, 0.000000000000000000, 0.000000000000000000 ) ) ;
#15957=DIRECTION ( 'NONE',  ( 0.000000000000000000, 0.000000000000000000, 1.000000000000000000 ) ) ;
#16000=LINE ( 'NONE', #12811, #11197 ) ;
#16048=CARTESIAN_POINT ( 'NONE',  ( 4.000000000000000000, 2.639212418033078489, 1.523749999999995053 ) ) ;
#16110=CARTESIAN_POINT ( 'NONE',  ( 0.000000000000000000, 0.000000000000000000, 0.000000000000000000 ) ) ;
#16117=EDGE_CURVE ( 'NONE', #12336, #15178, #12480, .T. ) ;
#16171=CARTESIAN_POINT ( 'NONE',  ( 0.000000000000000000, 1.759474945355379960, -3.047500000000001652 ) ) ;
#16196=ORIENTED_EDGE ( 'NONE', *, *, #9637, .T. ) ;
#16216=LINE ( 'NONE', #3375, #17813 ) ;
#16238=LINE ( 'NONE', #130, #2074 ) ;
#16260=ADVANCED_FACE ( 'NONE', ( #14396 ), #9689, .T. ) ;
#16269=FACE_OUTER_BOUND ( 'NONE', #645, .T. ) ;
#16296=VECTOR ( 'NONE', #15748, 1000.000000000000000 ) ;
#16311=CARTESIAN_POINT ( 'NONE',  ( 4.000000000000000000, -2.639212418033072716, 1.523750000000001492 ) ) ;
#16324=DIRECTION ( 'NONE',  ( 0.000000000000000000, 0.4999999999999985012, -0.8660254037844394848 ) ) ;
#16345=VECTOR ( 'NONE', #3921, 1000.000000000000000 ) ;
#16443=LINE ( 'NONE', #8696, #11990 ) ;
#16547=ORIENTED_EDGE ( 'NONE', *, *, #12757, .F. ) ;
#16578=DIRECTION ( 'NONE',  ( 0.000000000000000000, 0.000000000000000000, -1.000000000000000000 ) ) ;
#16580=ORIENTED_EDGE ( 'NONE', *, *, #7406, .F. ) ;
#16583=LINE ( 'NONE', #9985, #16977 ) ;
#16618=ADVANCED_FACE ( 'NONE', ( #8254, #11770 ), #18027, .T. ) ;
#16669=EDGE_LOOP ( 'NONE', ( #18050, #14245, #6576 ) ) ;
#16752=DIRECTION ( 'NONE',  ( -1.000000000000000000, -0.000000000000000000, -0.000000000000000000 ) ) ;
#16767=ORIENTED_EDGE ( 'NONE', *, *, #9637, .F. ) ;
#16793=ORIENTED_EDGE ( 'NONE', *, *, #14381, .F. ) ;
#16799=AXIS2_PLACEMENT_3D ( 'NONE', #17602, #11440, #6236 ) ;
#16804=EDGE_CURVE ( 'NONE', #3452, #18781, #15172, .T. ) ;
#16810=AXIS2_PLACEMENT_3D ( 'NONE', #16110, #19466, #19378 ) ;
#16852=CARTESIAN_POINT ( 'NONE',  ( 8.399999999999998579, 0.000000000000000000, 0.000000000000000000 ) ) ;
#16921=EDGE_CURVE ( 'NONE', #18021, #17399, #1580, .T. ) ;
#16925=LINE ( 'NONE', #4098, #1115 ) ;
#16947=EDGE_CURVE ( 'NONE', #3452, #15824, #15500, .T. ) ;
#16950=ORIENTED_EDGE ( 'NONE', *, *, #16921, .T. ) ;
#16964=AXIS2_PLACEMENT_3D ( 'NONE', #7754, #19114, #17312 ) ;
#16972=DIRECTION ( 'NONE',  ( -1.000000000000000000, -0.000000000000000000, -0.000000000000000000 ) ) ;
#16977=VECTOR ( 'NONE', #20079, 1000.000000000000000 ) ;
#17008=VERTEX_POINT ( 'NONE', #9820 ) ;
#17052=ADVANCED_FACE ( 'NONE', ( #18108 ), #19575, .T. ) ;
#17091=CIRCLE ( 'NONE', #4218, 3.309499999999999886 ) ;
#17130=ORIENTED_EDGE ( 'NONE', *, *, #20148, .T. ) ;
#17162=ORIENTED_EDGE ( 'NONE', *, *, #13104, .F. ) ;
#17221=LINE ( 'NONE', #8186, #1859 ) ;
#17253=DIRECTION ( 'NONE',  ( 0.000000000000000000, -0.4999999999999985567, 0.8660254037844393737 ) ) ;
#17281=MANIFOLD_SOLID_BREP ( 'Hex', #20157 ) ;
#17289=TOROIDAL_SURFACE ( 'NONE', #5763, 4.400000000000000355, 0.4000000000000000222 ) ;
#17299=AXIS2_PLACEMENT_3D ( 'NONE', #6315, #12494, #15789 ) ;
#17312=DIRECTION ( 'NONE',  ( 0.000000000000000000, 0.000000000000000000, -1.000000000000000000 ) ) ;
#17347=CARTESIAN_POINT ( 'NONE',  ( 8.399999999999998579, 0.000000000000000000, 0.000000000000000000 ) ) ;
#17365=LINE ( 'NONE', #3149, #10957 ) ;
#17399=VERTEX_POINT ( 'NONE', #17673 ) ;
#17403=PRODUCT_CONTEXT ( 'NONE', #927, 'mechanical' ) ;
#17414=DIRECTION ( 'NONE',  ( -1.000000000000000000, -0.000000000000000000, -0.000000000000000000 ) ) ;
#17430=PRODUCT_DEFINITION_CONTEXT ( 'detailed design', #4458, 'design' ) ;
#17442=EDGE_CURVE ( 'NONE', #18235, #11211, #6330, .T. ) ;
#17447=VERTEX_POINT ( 'NONE', #14165 ) ;
#17483=CARTESIAN_POINT ( 'NONE',  ( 4.000000000000000000, -3.518949890710766581, 4.553649124439118623E-15 ) ) ;
#17496=AXIS2_PLACEMENT_3D ( 'NONE', #3009, #20708, #15957 ) ;
#17524=EDGE_LOOP ( 'NONE', ( #5322, #13406, #10753, #1578 ) ) ;
#17539=DIRECTION ( 'NONE',  ( 0.000000000000000000, 0.000000000000000000, 1.000000000000000000 ) ) ;
#17602=CARTESIAN_POINT ( 'NONE',  ( 42.30949999999999989, 0.000000000000000000, 0.000000000000000000 ) ) ;
#17655=AXIS2_PLACEMENT_3D ( 'NONE', #15766, #18831, #9367 ) ;
#17673=CARTESIAN_POINT ( 'NONE',  ( 4.000000000000000000, -2.639212418033078045, -1.523749999999994831 ) ) ;
#17677=EDGE_CURVE ( 'NONE', #4969, #423, #2656, .T. ) ;
#17694=CARTESIAN_POINT ( 'NONE',  ( 7.999999999999998224, 0.000000000000000000, -4.400000000000000355 ) ) ;
#17697=DIRECTION ( 'NONE',  ( 0.000000000000000000, 0.000000000000000000, -1.000000000000000000 ) ) ;
#17722=SHAPE_DEFINITION_REPRESENTATION ( #13299, #6230 ) ;
#17761=DIRECTION ( 'NONE',  ( 0.000000000000000000, 0.000000000000000000, -1.000000000000000000 ) ) ;
#17791=CARTESIAN_POINT ( 'NONE',  ( 8.399999999999998579, 0.000000000000000000, 0.000000000000000000 ) ) ;
#17811=AXIS2_PLACEMENT_3D ( 'NONE', #10144, #13677, #10255 ) ;
#17813=VECTOR ( 'NONE', #6543, 1000.000000000000000 ) ;
#17836=CARTESIAN_POINT ( 'NONE',  ( 4.000000000000000000, -1.759474945355379072, 3.047500000000001652 ) ) ;
#17954=VERTEX_POINT ( 'NONE', #20484 ) ;
#17981=EDGE_CURVE ( 'NONE', #20478, #18457, #996, .T. ) ;
#18021=VERTEX_POINT ( 'NONE', #4280 ) ;
#18027=PLANE ( 'NONE',  #20537 ) ;
#18050=ORIENTED_EDGE ( 'NONE', *, *, #16921, .F. ) ;
#18051=ORIENTED_EDGE ( 'NONE', *, *, #3566, .T. ) ;
#18108=FACE_OUTER_BOUND ( 'NONE', #2783, .T. ) ;
#18131=CARTESIAN_POINT ( 'NONE',  ( 4.000000000000000000, 5.278424836066145431, -3.047500000000006093 ) ) ;
#18137=PLANE ( 'NONE',  #12676 ) ;
#18160=FACE_OUTER_BOUND ( 'NONE', #18592, .T. ) ;
#18188=LINE ( 'NONE', #13528, #8485 ) ;
#18201=MECHANICAL_DESIGN_GEOMETRIC_PRESENTATION_REPRESENTATION('',(#14167),#3630);
#18233=AXIS2_PLACEMENT_3D ( 'NONE', #15903, #1274, #19656 ) ;
#18235=VERTEX_POINT ( 'NONE', #2785 ) ;
#18240=CARTESIAN_POINT ( 'NONE',  ( 7.999999999999998224, 0.000000000000000000, 0.000000000000000000 ) ) ;
#18297=ORIENTED_EDGE ( 'NONE', *, *, #13935, .F. ) ;
#18357=AXIS2_PLACEMENT_3D ( 'NONE', #1287, #2771, #19189 ) ;
#18400=DIRECTION ( 'NONE',  ( -1.000000000000000000, -0.000000000000000000, -0.000000000000000000 ) ) ;
#18452=CARTESIAN_POINT ( 'NONE',  ( 4.000000000000000000, 0.000000000000000000, 3.047499999999999876 ) ) ;
#18457=VERTEX_POINT ( 'NONE', #6355 ) ;
#18508=AXIS2_PLACEMENT_3D ( 'NONE', #17483, #2959, #1368 ) ;
#18540=EDGE_LOOP ( 'NONE', ( #17130, #503 ) ) ;
#18552=DIRECTION ( 'NONE',  ( 0.000000000000000000, 0.000000000000000000, -1.000000000000000000 ) ) ;
#18553=ORIENTED_EDGE ( 'NONE', *, *, #17677, .F. ) ;
#18560=DIRECTION ( 'NONE',  ( 0.000000000000000000, 0.5000000000000009992, 0.8660254037844381525 ) ) ;
#18581=ADVANCED_FACE ( 'NONE', ( #11669 ), #13581, .F. ) ;
#18592=EDGE_LOOP ( 'NONE', ( #12640, #9094, #5292 ) ) ;
#18638=CARTESIAN_POINT ( 'NONE',  ( 4.000000000000000000, -1.759474945355387954, -3.047499999999997211 ) ) ;
#18781=VERTEX_POINT ( 'NONE', #7724 ) ;
#18831=DIRECTION ( 'NONE',  ( -1.000000000000000000, -0.000000000000000000, -0.000000000000000000 ) ) ;
#18866=ORIENTED_EDGE ( 'NONE', *, *, #7047, .F. ) ;
#18904=FACE_OUTER_BOUND ( 'NONE', #14252, .T. ) ;
#18909=DIRECTION ( 'NONE',  ( -1.000000000000000000, -0.000000000000000000, -0.000000000000000000 ) ) ;
#18958=ORIENTED_EDGE ( 'NONE', *, *, #13206, .T. ) ;
#18960=DIRECTION ( 'NONE',  ( 1.000000000000000000, 0.000000000000000000, 0.000000000000000000 ) ) ;
#18970=ORIENTED_EDGE ( 'NONE', *, *, #3087, .F. ) ;
#19043=DIRECTION ( 'NONE',  ( 0.000000000000000000, 0.000000000000000000, -1.000000000000000000 ) ) ;
#19068=ORIENTED_EDGE ( 'NONE', *, *, #9008, .T. ) ;
#19114=DIRECTION ( 'NONE',  ( 1.000000000000000000, 0.000000000000000000, 0.000000000000000000 ) ) ;
#19147=CARTESIAN_POINT ( 'NONE',  ( 4.000000000000000000, 3.518949890710767026, -4.987329993433320396E-15 ) ) ;
#19149=( NAMED_UNIT ( * ) PLANE_ANGLE_UNIT ( ) SI_UNIT ( $, .RADIAN. ) );
#19189=DIRECTION ( 'NONE',  ( 0.000000000000000000, 0.000000000000000000, -1.000000000000000000 ) ) ;
#19191=ORIENTED_EDGE ( 'NONE', *, *, #8242, .F. ) ;
#19208=CARTESIAN_POINT ( 'NONE',  ( 0.000000000000000000, 7.715274834628324392E-16, -6.099999999999999645 ) ) ;
#19259=VECTOR ( 'NONE', #678, 1000.000000000000000 ) ;
#19282=CARTESIAN_POINT ( 'NONE',  ( 8.399999999999998579, 0.000000000000000000, -4.400000000000000355 ) ) ;
#19288=AXIS2_PLACEMENT_3D ( 'NONE', #3586, #4868, #11756 ) ;
#19325=EDGE_LOOP ( 'NONE', ( #14182, #15150, #20150, #13443 ) ) ;
#19344=EDGE_CURVE ( 'NONE', #11275, #7000, #13319, .T. ) ;
#19378=DIRECTION ( 'NONE',  ( -0.000000000000000000, 0.000000000000000000, 1.000000000000000000 ) ) ;
#19379=ORIENTED_EDGE ( 'NONE', *, *, #19344, .T. ) ;
#19412=DIRECTION ( 'NONE',  ( 0.000000000000000000, -1.000000000000000000, 1.355657144061424088E-15 ) ) ;
#19466=DIRECTION ( 'NONE',  ( -1.000000000000000000, 0.000000000000000000, -0.000000000000000000 ) ) ;
#19529=DIRECTION ( 'NONE',  ( -1.000000000000000000, -0.000000000000000000, -0.000000000000000000 ) ) ;
#19572=FACE_BOUND ( 'NONE', #14414, .T. ) ;
#19575=CYLINDRICAL_SURFACE ( 'NONE', #13457, 4.000000000000000000 ) ;
#19579=PRODUCT_DEFINITION_FORMATION_WITH_SPECIFIED_SOURCE ( 'ANY', '', #13821, .NOT_KNOWN. ) ;
#19602=DIRECTION ( 'NONE',  ( 0.000000000000000000, 0.000000000000000000, 1.000000000000000000 ) ) ;
#19610=FACE_OUTER_BOUND ( 'NONE', #1044, .T. ) ;
#19656=DIRECTION ( 'NONE',  ( 1.000000000000000000, 0.000000000000000000, 0.000000000000000000 ) ) ;
#19710=CARTESIAN_POINT ( 'NONE',  ( 0.3999999999999975797, 0.000000000000000000, 0.000000000000000000 ) ) ;
#19825=VECTOR ( 'NONE', #15479, 1000.000000000000000 ) ;
#19833=CIRCLE ( 'NONE', #4278, 3.047499999999999876 ) ;
#19838=DIRECTION ( 'NONE',  ( -1.000000000000000000, -0.000000000000000000, -0.000000000000000000 ) ) ;
#19908=ORIENTED_EDGE ( 'NONE', *, *, #2048, .T. ) ;
#19986=ORIENTED_EDGE ( 'NONE', *, *, #1923, .F. ) ;
#20011=LINE ( 'NONE', #11859, #10939 ) ;
#20039=LINE ( 'NONE', #18452, #16345 ) ;
#20065=ORIENTED_EDGE ( 'NONE', *, *, #3566, .F. ) ;
#20079=DIRECTION ( 'NONE',  ( 0.000000000000000000, -0.5000000000000009992, -0.8660254037844380415 ) ) ;
#20148=EDGE_CURVE ( 'NONE', #17008, #14920, #592, .T. ) ;
#20149=AXIS2_PLACEMENT_3D ( 'NONE', #19710, #16752, #439 ) ;
#20150=ORIENTED_EDGE ( 'NONE', *, *, #13923, .T. ) ;
#20157=CLOSED_SHELL ( 'NONE', ( #12015, #3806, #15870, #729, #16260, #14348, #15779, #2801, #16618, #17052, #15076, #1273, #5468, #14991, #2478, #13535, #9922, #15767, #11739, #13650, #9464, #18581, #2207, #14612, #6535, #6177, #13593 ) ) ;
#20160=FACE_OUTER_BOUND ( 'NONE', #4047, .T. ) ;
#20223=AXIS2_PLACEMENT_3D ( 'NONE', #2920, #7985, #3126 ) ;
#20230=VERTEX_POINT ( 'NONE', #16171 ) ;
#20297=CARTESIAN_POINT ( 'NONE',  ( 8.399999999999998579, 4.898587196589412829E-16, -4.000000000000000000 ) ) ;
#20381=CARTESIAN_POINT ( 'NONE',  ( 4.000000000000000000, -1.759474945355387954, -3.047499999999997211 ) ) ;
#20398=( LENGTH_UNIT ( ) NAMED_UNIT ( * ) SI_UNIT ( .MILLI., .METRE. ) );
#20440=DIRECTION ( 'NONE',  ( 0.000000000000000000, 0.000000000000000000, -1.000000000000000000 ) ) ;
#20478=VERTEX_POINT ( 'NONE', #13298 ) ;
#20481=LINE ( 'NONE', #2800, #7797 ) ;
#20484=CARTESIAN_POINT ( 'NONE',  ( 0.000000000000000000, -3.518949890710766581, 4.553649124439118623E-15 ) ) ;
#20537=AXIS2_PLACEMENT_3D ( 'NONE', #3694, #10148, #3496 ) ;
#20610=CARTESIAN_POINT ( 'NONE',  ( 0.3999999999999975797, 0.000000000000000000, 0.000000000000000000 ) ) ;
#20638=VERTEX_POINT ( 'NONE', #11916 ) ;
#20640=CARTESIAN_POINT ( 'NONE',  ( 4.000000000000000000, 1.759474945355388398, 3.047499999999996767 ) ) ;
#20644=EDGE_LOOP ( 'NONE', ( #4552, #15765 ) ) ;
#20652=CARTESIAN_POINT ( 'NONE',  ( 4.000000000000000000, 0.000000000000000000, 0.000000000000000000 ) ) ;
#20708=DIRECTION ( 'NONE',  ( -1.000000000000000000, -0.000000000000000000, -0.000000000000000000 ) ) ;
#20744=DIRECTION ( 'NONE',  ( 0.000000000000000000, -1.000000000000000000, 1.232415585510385534E-15 ) ) ;
#20821=CONICAL_SURFACE ( 'NONE', #1547, 3.309499999999999886, 0.7853981633974501664 ) ;
#20849=CARTESIAN_POINT ( 'NONE',  ( 0.000000000000000000, 1.759474945355388398, 3.047499999999996767 ) ) ;
#20852=TOROIDAL_SURFACE ( 'NONE', #8316, 4.400000000000000355, 0.4000000000000000222 ) ;
#20875=ORIENTED_EDGE ( 'NONE', *, *, #9008, .F. ) ;
#20881=DIRECTION ( 'NONE',  ( 0.000000000000000000, -0.8660254037844394848, -0.4999999999999986122 ) ) ;
#20989=COLOUR_RGB('Black',0.12,0.14,0.17);
#20990=FILL_AREA_STYLE_COLOUR('',#20989);
#20991=FILL_AREA_STYLE('',(#20990));
#20992=SURFACE_STYLE_FILL_AREA(#20991);
#20993=SURFACE_SIDE_STYLE('',(#20992));
#20994=SURFACE_STYLE_USAGE(.BOTH.,#20993);
#20995=PRESENTATION_STYLE_ASSIGNMENT((#20994));
ENDSEC;
END-ISO-10303-21;
